ISO-10303-21;
HEADER;
/* Generated by software containing ST-Developer
 * from STEP Tools, Inc. (www.steptools.com) 
 */

FILE_DESCRIPTION(
/* description */ ('Hand drill press frame (manual)'),
/* implementation_level */ '2;1');

FILE_NAME(
/* name */ 'M4 tool retaining screw.step',
/* time_stamp */ '2026-10-28T03:25:28-07:00',
/* author */ (''),
/* organization */ (''),
/* preprocessor_version */ 'ST-DEVELOPER v20.2',
/* originating_system */ 'Autodesk Translation Framework v15.17.0.0',
/* authorisation */ '');

FILE_SCHEMA (('AUTOMOTIVE_DESIGN { 1 0 10303 214 3 1 1 }'));
ENDSEC;

DATA;
#10=MECHANICAL_DESIGN_GEOMETRIC_PRESENTATION_REPRESENTATION('',(#652),#33299);
#555=SHAPE_REPRESENTATION_RELATIONSHIP('SRR','None',#33516,#600);
#600=ADVANCED_BREP_SHAPE_REPRESENTATION('',(#703),#33278);
#652=STYLED_ITEM('',(#33821),#703);
#703=MANIFOLD_SOLID_BREP('Body1',#12671);
#1221=PLANE('',#13965);
#1222=PLANE('',#13966);
#1804=FACE_OUTER_BOUND('',#2625,.T.);
#1805=FACE_OUTER_BOUND('',#2626,.T.);
#1806=FACE_OUTER_BOUND('',#2627,.T.);
#2625=EDGE_LOOP('',(#10763,#10764,#10765,#10766));
#2626=EDGE_LOOP('',(#10767));
#2627=EDGE_LOOP('',(#10768));
#3748=LINE('',#20884,#4913);
#4913=VECTOR('',#16783,0.199999999999999);
#5487=CIRCLE('',#13963,0.199999999999999);
#5488=CIRCLE('',#13964,0.199999999999999);
#6401=VERTEX_POINT('',#20881);
#6402=VERTEX_POINT('',#20883);
#7910=EDGE_CURVE('',#6401,#6401,#5487,.T.);
#7911=EDGE_CURVE('',#6401,#6402,#3748,.T.);
#7912=EDGE_CURVE('',#6402,#6402,#5488,.T.);
#10763=ORIENTED_EDGE('',*,*,#7910,.F.);
#10764=ORIENTED_EDGE('',*,*,#7911,.T.);
#10765=ORIENTED_EDGE('',*,*,#7912,.T.);
#10766=ORIENTED_EDGE('',*,*,#7911,.F.);
#10767=ORIENTED_EDGE('',*,*,#7910,.T.);
#10768=ORIENTED_EDGE('',*,*,#7912,.F.);
#11892=CYLINDRICAL_SURFACE('',#13962,0.199999999999999);
#12413=ADVANCED_FACE('',(#1804),#11892,.T.);
#12414=ADVANCED_FACE('',(#1805),#1221,.T.);
#12415=ADVANCED_FACE('',(#1806),#1222,.F.);
#12671=CLOSED_SHELL('',(#12413,#12414,#12415));
#13961=AXIS2_PLACEMENT_3D('',#20879,#16777,#16778);
#13962=AXIS2_PLACEMENT_3D('',#20880,#16779,#16780);
#13963=AXIS2_PLACEMENT_3D('',#20882,#16781,#16782);
#13964=AXIS2_PLACEMENT_3D('',#20885,#16784,#16785);
#13965=AXIS2_PLACEMENT_3D('',#20886,#16786,#16787);
#13966=AXIS2_PLACEMENT_3D('',#20887,#16788,#16789);
#16777=DIRECTION('axis',(0.,0.,1.));
#16778=DIRECTION('refdir',(1.,0.,0.));
#16779=DIRECTION('center_axis',(1.,0.,0.));
#16780=DIRECTION('ref_axis',(0.,0.,-1.));
#16781=DIRECTION('center_axis',(1.,0.,0.));
#16782=DIRECTION('ref_axis',(0.,0.,-1.));
#16783=DIRECTION('',(-1.,0.,0.));
#16784=DIRECTION('center_axis',(1.,0.,0.));
#16785=DIRECTION('ref_axis',(0.,0.,-1.));
#16786=DIRECTION('center_axis',(1.,0.,0.));
#16787=DIRECTION('ref_axis',(0.,0.,-1.));
#16788=DIRECTION('center_axis',(1.,0.,0.));
#16789=DIRECTION('ref_axis',(0.,0.,-1.));
#20879=CARTESIAN_POINT('',(0.,0.,0.));
#20880=CARTESIAN_POINT('Origin',(1.3,0.,10.4));
#20881=CARTESIAN_POINT('',(2.4,-2.4492935982947E-17,10.6));
#20882=CARTESIAN_POINT('Origin',(2.4,0.,10.4));
#20883=CARTESIAN_POINT('',(1.3,-2.4492935982947E-17,10.6));
#20884=CARTESIAN_POINT('',(1.3,-2.4492935982947E-17,10.6));
#20885=CARTESIAN_POINT('Origin',(1.3,0.,10.4));
#20886=CARTESIAN_POINT('Origin',(2.4,0.,10.4));
#20887=CARTESIAN_POINT('Origin',(1.3,0.,10.4));
#33226=UNCERTAINTY_MEASURE_WITH_UNIT(LENGTH_MEASURE(0.001),#33300,
'DISTANCE_ACCURACY_VALUE',
'Maximum model space distance between geometric entities at asserted c
onnectivities');
#33247=UNCERTAINTY_MEASURE_WITH_UNIT(LENGTH_MEASURE(0.001),#33300,
'DISTANCE_ACCURACY_VALUE',
'Maximum model space distance between geometric entities at asserted c
onnectivities');
#33278=(
GEOMETRIC_REPRESENTATION_CONTEXT(3)
GLOBAL_UNCERTAINTY_ASSIGNED_CONTEXT((#33226))
GLOBAL_UNIT_ASSIGNED_CONTEXT((#33300,#33302,#33303))
REPRESENTATION_CONTEXT('','3D')
);
#33299=(
GEOMETRIC_REPRESENTATION_CONTEXT(3)
GLOBAL_UNCERTAINTY_ASSIGNED_CONTEXT((#33247))
GLOBAL_UNIT_ASSIGNED_CONTEXT((#33300,#33302,#33303))
REPRESENTATION_CONTEXT('','3D')
);
#33300=(
LENGTH_UNIT()
NAMED_UNIT(*)
SI_UNIT(.CENTI.,.METRE.)
);
#33302=(
NAMED_UNIT(*)
PLANE_ANGLE_UNIT()
SI_UNIT($,.RADIAN.)
);
#33303=(
NAMED_UNIT(*)
SI_UNIT($,.STERADIAN.)
SOLID_ANGLE_UNIT()
);
#33334=SHAPE_DEFINITION_REPRESENTATION(#33390,#33516);
#33390=PRODUCT_DEFINITION_SHAPE('',$,#33568);
#33516=SHAPE_REPRESENTATION('',(#13961),#33278);
#33537=PRODUCT_DEFINITION_CONTEXT('part definition',#33692,'design');
#33568=PRODUCT_DEFINITION('M4 tool retaining screw',
'M4 tool retaining screw',#33619,#33537);
#33619=PRODUCT_DEFINITION_FORMATION('',$,#33724);
#33692=APPLICATION_CONTEXT(
'Core Data for Automotive Mechanical Design Process');
#33693=PRODUCT_CONTEXT('part definition',#33692,'mechanical');
#33724=PRODUCT('M4 tool retaining screw','M4 tool retaining screw',
'M4 tool retaining screw',(#33693));
#33815=COLOUR_RGB('Black',0.12,0.14,0.17);
#33816=FILL_AREA_STYLE_COLOUR('',#33815);
#33817=FILL_AREA_STYLE('',(#33816));
#33818=SURFACE_STYLE_FILL_AREA(#33817);
#33819=SURFACE_SIDE_STYLE('',(#33818));
#33820=SURFACE_STYLE_USAGE(.BOTH.,#33819);
#33821=PRESENTATION_STYLE_ASSIGNMENT((#33820));
ENDSEC;
END-ISO-10303-21;
